ISO-10303-21;
HEADER;
/* Generated by software containing ST-Developer
 * from STEP Tools, Inc. (www.steptools.com) 
 */

FILE_DESCRIPTION(
/* description */ ('PAT-091'),
/* implementation_level */ '2;1');

FILE_NAME(
/* name */ 'Axle end keeper (3).step',
/* time_stamp */ '2026-10-27T15:34:44-07:00',
/* author */ (''),
/* organization */ (''),
/* preprocessor_version */ 'ST-DEVELOPER v20.2',
/* originating_system */ 'Autodesk Translation Framework v15.17.0.0',
/* authorisation */ '');

FILE_SCHEMA (('AUTOMOTIVE_DESIGN { 1 0 10303 214 3 1 1 }'));
ENDSEC;

DATA;
#10=MECHANICAL_DESIGN_GEOMETRIC_PRESENTATION_REPRESENTATION('',(#996),#25100);
#776=SHAPE_REPRESENTATION_RELATIONSHIP('SRR','None',#25538,#886);
#886=ADVANCED_BREP_SHAPE_REPRESENTATION('',(#1119),#25008);
#996=STYLED_ITEM('',(#26191),#1119);
#1119=MANIFOLD_SOLID_BREP('Body1',#13274);
#1381=FACE_BOUND('',#3273,.T.);
#1382=FACE_BOUND('',#3275,.T.);
#1756=PLANE('',#15054);
#1757=PLANE('',#15055);
#2286=FACE_OUTER_BOUND('',#3270,.T.);
#2287=FACE_OUTER_BOUND('',#3271,.T.);
#2288=FACE_OUTER_BOUND('',#3272,.T.);
#2289=FACE_OUTER_BOUND('',#3274,.T.);
#3270=EDGE_LOOP('',(#9932,#9933,#9934,#9935));
#3271=EDGE_LOOP('',(#9936,#9937,#9938,#9939));
#3272=EDGE_LOOP('',(#9940));
#3273=EDGE_LOOP('',(#9941));
#3274=EDGE_LOOP('',(#9942));
#3275=EDGE_LOOP('',(#9943));
#4393=LINE('',#22029,#5133);
#4394=LINE('',#22035,#5134);
#5133=VECTOR('',#17667,0.225);
#5134=VECTOR('',#17674,1.);
#5815=CIRCLE('',#15049,0.225);
#5816=CIRCLE('',#15050,0.225);
#5817=CIRCLE('',#15052,1.);
#5818=CIRCLE('',#15053,1.);
#6702=VERTEX_POINT('',#22026);
#6703=VERTEX_POINT('',#22028);
#6704=VERTEX_POINT('',#22032);
#6705=VERTEX_POINT('',#22034);
#7901=EDGE_CURVE('',#6702,#6702,#5815,.T.);
#7902=EDGE_CURVE('',#6702,#6703,#4393,.T.);
#7903=EDGE_CURVE('',#6703,#6703,#5816,.T.);
#7904=EDGE_CURVE('',#6704,#6704,#5817,.T.);
#7905=EDGE_CURVE('',#6704,#6705,#4394,.T.);
#7906=EDGE_CURVE('',#6705,#6705,#5818,.T.);
#9932=ORIENTED_EDGE('',*,*,#7901,.F.);
#9933=ORIENTED_EDGE('',*,*,#7902,.T.);
#9934=ORIENTED_EDGE('',*,*,#7903,.T.);
#9935=ORIENTED_EDGE('',*,*,#7902,.F.);
#9936=ORIENTED_EDGE('',*,*,#7904,.F.);
#9937=ORIENTED_EDGE('',*,*,#7905,.T.);
#9938=ORIENTED_EDGE('',*,*,#7906,.T.);
#9939=ORIENTED_EDGE('',*,*,#7905,.F.);
#9940=ORIENTED_EDGE('',*,*,#7904,.T.);
#9941=ORIENTED_EDGE('',*,*,#7901,.T.);
#9942=ORIENTED_EDGE('',*,*,#7906,.F.);
#9943=ORIENTED_EDGE('',*,*,#7903,.F.);
#12178=CYLINDRICAL_SURFACE('',#15048,0.225);
#12179=CYLINDRICAL_SURFACE('',#15051,1.);
#12653=ADVANCED_FACE('',(#2286),#12178,.F.);
#12654=ADVANCED_FACE('',(#2287),#12179,.T.);
#12655=ADVANCED_FACE('',(#2288,#1381),#1756,.T.);
#12656=ADVANCED_FACE('',(#2289,#1382),#1757,.F.);
#13274=CLOSED_SHELL('',(#12653,#12654,#12655,#12656));
#15047=AXIS2_PLACEMENT_3D('',#22024,#17661,#17662);
#15048=AXIS2_PLACEMENT_3D('',#22025,#17663,#17664);
#15049=AXIS2_PLACEMENT_3D('',#22027,#17665,#17666);
#15050=AXIS2_PLACEMENT_3D('',#22030,#17668,#17669);
#15051=AXIS2_PLACEMENT_3D('',#22031,#17670,#17671);
#15052=AXIS2_PLACEMENT_3D('',#22033,#17672,#17673);
#15053=AXIS2_PLACEMENT_3D('',#22036,#17675,#17676);
#15054=AXIS2_PLACEMENT_3D('',#22037,#17677,#17678);
#15055=AXIS2_PLACEMENT_3D('',#22038,#17679,#17680);
#17661=DIRECTION('axis',(0.,0.,1.));
#17662=DIRECTION('refdir',(1.,0.,0.));
#17663=DIRECTION('center_axis',(0.,1.,0.));
#17664=DIRECTION('ref_axis',(1.,0.,0.));
#17665=DIRECTION('center_axis',(0.,-1.,0.));
#17666=DIRECTION('ref_axis',(1.,0.,0.));
#17667=DIRECTION('',(0.,-1.,0.));
#17668=DIRECTION('center_axis',(0.,-1.,0.));
#17669=DIRECTION('ref_axis',(1.,0.,0.));
#17670=DIRECTION('center_axis',(0.,1.,0.));
#17671=DIRECTION('ref_axis',(1.,0.,0.));
#17672=DIRECTION('center_axis',(0.,1.,0.));
#17673=DIRECTION('ref_axis',(1.,0.,0.));
#17674=DIRECTION('',(0.,-1.,0.));
#17675=DIRECTION('center_axis',(0.,1.,0.));
#17676=DIRECTION('ref_axis',(1.,0.,0.));
#17677=DIRECTION('center_axis',(0.,1.,0.));
#17678=DIRECTION('ref_axis',(1.,0.,0.));
#17679=DIRECTION('center_axis',(0.,1.,0.));
#17680=DIRECTION('ref_axis',(1.,0.,0.));
#22024=CARTESIAN_POINT('',(0.,0.,0.));
#22025=CARTESIAN_POINT('Origin',(0.,8.5,13.));
#22026=CARTESIAN_POINT('',(-0.225,8.7,13.));
#22027=CARTESIAN_POINT('Origin',(0.,8.7,13.));
#22028=CARTESIAN_POINT('',(-0.225,8.5,13.));
#22029=CARTESIAN_POINT('',(-0.225,8.5,13.));
#22030=CARTESIAN_POINT('Origin',(0.,8.5,13.));
#22031=CARTESIAN_POINT('Origin',(0.,8.5,13.));
#22032=CARTESIAN_POINT('',(-1.,8.7,13.));
#22033=CARTESIAN_POINT('Origin',(0.,8.7,13.));
#22034=CARTESIAN_POINT('',(-1.,8.5,13.));
#22035=CARTESIAN_POINT('',(-1.,8.5,13.));
#22036=CARTESIAN_POINT('Origin',(0.,8.5,13.));
#22037=CARTESIAN_POINT('Origin',(0.,8.7,13.));
#22038=CARTESIAN_POINT('Origin',(0.,8.5,13.));
#24887=UNCERTAINTY_MEASURE_WITH_UNIT(LENGTH_MEASURE(0.001),#25101,
'DISTANCE_ACCURACY_VALUE',
'Maximum model space distance between geometric entities at asserted c
onnectivities');
#24979=UNCERTAINTY_MEASURE_WITH_UNIT(LENGTH_MEASURE(0.001),#25101,
'DISTANCE_ACCURACY_VALUE',
'Maximum model space distance between geometric entities at asserted c
onnectivities');
#25008=(
GEOMETRIC_REPRESENTATION_CONTEXT(3)
GLOBAL_UNCERTAINTY_ASSIGNED_CONTEXT((#24887))
GLOBAL_UNIT_ASSIGNED_CONTEXT((#25101,#25103,#25104))
REPRESENTATION_CONTEXT('','3D')
);
#25100=(
GEOMETRIC_REPRESENTATION_CONTEXT(3)
GLOBAL_UNCERTAINTY_ASSIGNED_CONTEXT((#24979))
GLOBAL_UNIT_ASSIGNED_CONTEXT((#25101,#25103,#25104))
REPRESENTATION_CONTEXT('','3D')
);
#25101=(
LENGTH_UNIT()
NAMED_UNIT(*)
SI_UNIT(.CENTI.,.METRE.)
);
#25103=(
NAMED_UNIT(*)
PLANE_ANGLE_UNIT()
SI_UNIT($,.RADIAN.)
);
#25104=(
NAMED_UNIT(*)
SI_UNIT($,.STERADIAN.)
SOLID_ANGLE_UNIT()
);
#25133=SHAPE_DEFINITION_REPRESENTATION(#25253,#25538);
#25253=PRODUCT_DEFINITION_SHAPE('',$,#25659);
#25538=SHAPE_REPRESENTATION('',(#15047),#25008);
#25630=PRODUCT_DEFINITION_CONTEXT('part definition',#25992,'design');
#25659=PRODUCT_DEFINITION('Axle end keeper (3)','Axle end keeper (3)',#25779,
#25630);
#25779=PRODUCT_DEFINITION_FORMATION('',$,#26022);
#25992=APPLICATION_CONTEXT(
'Core Data for Automotive Mechanical Design Process');
#25993=PRODUCT_CONTEXT('part definition',#25992,'mechanical');
#26022=PRODUCT('Axle end keeper (3)','Axle end keeper (3)',
'Axle end keeper (3)',(#25993));
#26185=COLOUR_RGB('Grey',0.48,0.52,0.57);
#26186=FILL_AREA_STYLE_COLOUR('',#26185);
#26187=FILL_AREA_STYLE('',(#26186));
#26188=SURFACE_STYLE_FILL_AREA(#26187);
#26189=SURFACE_SIDE_STYLE('',(#26188));
#26190=SURFACE_STYLE_USAGE(.BOTH.,#26189);
#26191=PRESENTATION_STYLE_ASSIGNMENT((#26190));
ENDSEC;
END-ISO-10303-21;
